ISO-10303-21;
HEADER;
/* Generated by software containing ST-Developer
 * from STEP Tools, Inc. (www.steptools.com) 
 */

FILE_DESCRIPTION(
/* description */ ('Four-valve pipe header'),
/* implementation_level */ '2;1');

FILE_NAME(
/* name */ 'Hex Nut - M5.step',
/* time_stamp */ '2026-10-29T16:56:19-07:00',
/* author */ (''),
/* organization */ (''),
/* preprocessor_version */ 'ST-DEVELOPER v20.2',
/* originating_system */ 'Autodesk Translation Framework v15.17.0.0',
/* authorisation */ '');

FILE_SCHEMA (('AUTOMOTIVE_DESIGN { 1 0 10303 214 3 1 1 }'));
ENDSEC;

DATA;
#10=MECHANICAL_DESIGN_GEOMETRIC_PRESENTATION_REPRESENTATION('',(#348),#10119);
#252=(
BOUNDED_CURVE()
B_SPLINE_CURVE(2,(#9474,#9475,#9476),.UNSPECIFIED.,.F.,.F.)
B_SPLINE_CURVE_WITH_KNOTS((3,3),(0.140651836354967,0.670383167684795),
 .UNSPECIFIED.)
CURVE()
GEOMETRIC_REPRESENTATION_ITEM()
RATIONAL_B_SPLINE_CURVE((1.11602540378444,1.28867513459481,1.11602540378444))
REPRESENTATION_ITEM('')
);
#253=(
BOUNDED_CURVE()
B_SPLINE_CURVE(2,(#9478,#9479,#9480),.UNSPECIFIED.,.F.,.F.)
B_SPLINE_CURVE_WITH_KNOTS((3,3),(0.140651836354967,0.670383167684795),
 .UNSPECIFIED.)
CURVE()
GEOMETRIC_REPRESENTATION_ITEM()
RATIONAL_B_SPLINE_CURVE((1.11602540378444,1.28867513459481,1.11602540378444))
REPRESENTATION_ITEM('')
);
#254=(
BOUNDED_CURVE()
B_SPLINE_CURVE(2,(#9485,#9486,#9487),.UNSPECIFIED.,.F.,.F.)
B_SPLINE_CURVE_WITH_KNOTS((3,3),(0.140651836354967,0.670383167684795),
 .UNSPECIFIED.)
CURVE()
GEOMETRIC_REPRESENTATION_ITEM()
RATIONAL_B_SPLINE_CURVE((1.11602540378444,1.28867513459481,1.11602540378444))
REPRESENTATION_ITEM('')
);
#255=(
BOUNDED_CURVE()
B_SPLINE_CURVE(2,(#9489,#9490,#9491),.UNSPECIFIED.,.F.,.F.)
B_SPLINE_CURVE_WITH_KNOTS((3,3),(0.140651836354967,0.670383167684795),
 .UNSPECIFIED.)
CURVE()
GEOMETRIC_REPRESENTATION_ITEM()
RATIONAL_B_SPLINE_CURVE((1.11602540378444,1.28867513459481,1.11602540378444))
REPRESENTATION_ITEM('')
);
#256=(
BOUNDED_CURVE()
B_SPLINE_CURVE(2,(#9493,#9494,#9495),.UNSPECIFIED.,.F.,.F.)
B_SPLINE_CURVE_WITH_KNOTS((3,3),(0.140651836354967,0.670383167684795),
 .UNSPECIFIED.)
CURVE()
GEOMETRIC_REPRESENTATION_ITEM()
RATIONAL_B_SPLINE_CURVE((1.11602540378444,1.28867513459481,1.11602540378444))
REPRESENTATION_ITEM('')
);
#257=(
BOUNDED_CURVE()
B_SPLINE_CURVE(2,(#9496,#9497,#9498),.UNSPECIFIED.,.F.,.F.)
B_SPLINE_CURVE_WITH_KNOTS((3,3),(0.140651836354967,0.670383167684795),
 .UNSPECIFIED.)
CURVE()
GEOMETRIC_REPRESENTATION_ITEM()
RATIONAL_B_SPLINE_CURVE((1.11602540378444,1.28867513459481,1.11602540378444))
REPRESENTATION_ITEM('')
);
#258=(
BOUNDED_CURVE()
B_SPLINE_CURVE(2,(#9505,#9506,#9507),.UNSPECIFIED.,.F.,.F.)
B_SPLINE_CURVE_WITH_KNOTS((3,3),(0.140651836354967,0.670383167684795),
 .UNSPECIFIED.)
CURVE()
GEOMETRIC_REPRESENTATION_ITEM()
RATIONAL_B_SPLINE_CURVE((1.11602540378444,1.28867513459481,1.11602540378444))
REPRESENTATION_ITEM('')
);
#259=(
BOUNDED_CURVE()
B_SPLINE_CURVE(2,(#9509,#9510,#9511),.UNSPECIFIED.,.F.,.F.)
B_SPLINE_CURVE_WITH_KNOTS((3,3),(0.140651836354967,0.670383167684796),
 .UNSPECIFIED.)
CURVE()
GEOMETRIC_REPRESENTATION_ITEM()
RATIONAL_B_SPLINE_CURVE((1.11602540378444,1.28867513459481,1.11602540378444))
REPRESENTATION_ITEM('')
);
#260=(
BOUNDED_CURVE()
B_SPLINE_CURVE(2,(#9513,#9514,#9515),.UNSPECIFIED.,.F.,.F.)
B_SPLINE_CURVE_WITH_KNOTS((3,3),(0.140651836354967,0.670383167684795),
 .UNSPECIFIED.)
CURVE()
GEOMETRIC_REPRESENTATION_ITEM()
RATIONAL_B_SPLINE_CURVE((1.11602540378444,1.28867513459481,1.11602540378444))
REPRESENTATION_ITEM('')
);
#261=(
BOUNDED_CURVE()
B_SPLINE_CURVE(2,(#9517,#9518,#9519),.UNSPECIFIED.,.F.,.F.)
B_SPLINE_CURVE_WITH_KNOTS((3,3),(0.140651836354967,0.670383167684795),
 .UNSPECIFIED.)
CURVE()
GEOMETRIC_REPRESENTATION_ITEM()
RATIONAL_B_SPLINE_CURVE((1.11602540378444,1.28867513459482,1.11602540378444))
REPRESENTATION_ITEM('')
);
#262=(
BOUNDED_CURVE()
B_SPLINE_CURVE(2,(#9521,#9522,#9523),.UNSPECIFIED.,.F.,.F.)
B_SPLINE_CURVE_WITH_KNOTS((3,3),(0.140651836354967,0.670383167684795),
 .UNSPECIFIED.)
CURVE()
GEOMETRIC_REPRESENTATION_ITEM()
RATIONAL_B_SPLINE_CURVE((1.11602540378444,1.28867513459481,1.11602540378444))
REPRESENTATION_ITEM('')
);
#263=(
BOUNDED_CURVE()
B_SPLINE_CURVE(2,(#9524,#9525,#9526),.UNSPECIFIED.,.F.,.F.)
B_SPLINE_CURVE_WITH_KNOTS((3,3),(0.140651836354967,0.670383167684795),
 .UNSPECIFIED.)
CURVE()
GEOMETRIC_REPRESENTATION_ITEM()
RATIONAL_B_SPLINE_CURVE((1.11602540378444,1.28867513459481,1.11602540378444))
REPRESENTATION_ITEM('')
);
#270=CONICAL_SURFACE('',#6330,0.47094010767585,1.0471975511966);
#271=CONICAL_SURFACE('',#6332,0.47094010767585,1.0471975511966);
#296=SHAPE_REPRESENTATION_RELATIONSHIP('SRR','None',#10258,#322);
#322=ADVANCED_BREP_SHAPE_REPRESENTATION('',(#373),#10107);
#348=STYLED_ITEM('',(#10477),#373);
#373=MANIFOLD_SOLID_BREP('Body1',#5595);
#517=FACE_BOUND('',#1397,.T.);
#518=FACE_BOUND('',#1399,.T.);
#660=PLANE('',#6334);
#661=PLANE('',#6335);
#662=PLANE('',#6336);
#663=PLANE('',#6340);
#664=PLANE('',#6341);
#665=PLANE('',#6342);
#666=PLANE('',#6343);
#667=PLANE('',#6344);
#964=FACE_OUTER_BOUND('',#1387,.T.);
#965=FACE_OUTER_BOUND('',#1388,.T.);
#966=FACE_OUTER_BOUND('',#1389,.T.);
#967=FACE_OUTER_BOUND('',#1390,.T.);
#968=FACE_OUTER_BOUND('',#1391,.T.);
#969=FACE_OUTER_BOUND('',#1392,.T.);
#970=FACE_OUTER_BOUND('',#1393,.T.);
#971=FACE_OUTER_BOUND('',#1394,.T.);
#972=FACE_OUTER_BOUND('',#1395,.T.);
#973=FACE_OUTER_BOUND('',#1396,.T.);
#974=FACE_OUTER_BOUND('',#1398,.T.);
#1387=EDGE_LOOP('',(#4685,#4686,#4687,#4688,#4689,#4690,#4691,#4692,#4693));
#1388=EDGE_LOOP('',(#4694,#4695,#4696,#4697,#4698,#4699,#4700,#4701,#4702));
#1389=EDGE_LOOP('',(#4703,#4704,#4705,#4706));
#1390=EDGE_LOOP('',(#4707,#4708,#4709,#4710));
#1391=EDGE_LOOP('',(#4711,#4712,#4713,#4714));
#1392=EDGE_LOOP('',(#4715,#4716,#4717,#4718));
#1393=EDGE_LOOP('',(#4719,#4720,#4721,#4722));
#1394=EDGE_LOOP('',(#4723,#4724,#4725,#4726));
#1395=EDGE_LOOP('',(#4727,#4728,#4729,#4730));
#1396=EDGE_LOOP('',(#4731));
#1397=EDGE_LOOP('',(#4732));
#1398=EDGE_LOOP('',(#4733));
#1399=EDGE_LOOP('',(#4734));
#1775=LINE('',#9482,#2193);
#1776=LINE('',#9503,#2194);
#1777=LINE('',#9528,#2195);
#1778=LINE('',#9529,#2196);
#1779=LINE('',#9531,#2197);
#1780=LINE('',#9533,#2198);
#1781=LINE('',#9538,#2199);
#1782=LINE('',#9541,#2200);
#1783=LINE('',#9543,#2201);
#2193=VECTOR('',#7696,0.47094010767585);
#2194=VECTOR('',#7703,0.47094010767585);
#2195=VECTOR('',#7706,1.);
#2196=VECTOR('',#7707,1.);
#2197=VECTOR('',#7710,1.);
#2198=VECTOR('',#7713,1.);
#2199=VECTOR('',#7718,0.25);
#2200=VECTOR('',#7723,1.);
#2201=VECTOR('',#7726,1.);
#2523=CIRCLE('',#6331,0.38);
#2524=CIRCLE('',#6333,0.38);
#2525=CIRCLE('',#6338,0.2117);
#2526=CIRCLE('',#6339,0.2117);
#2888=VERTEX_POINT('',#9472);
#2889=VERTEX_POINT('',#9473);
#2890=VERTEX_POINT('',#9477);
#2891=VERTEX_POINT('',#9481);
#2892=VERTEX_POINT('',#9484);
#2893=VERTEX_POINT('',#9488);
#2894=VERTEX_POINT('',#9492);
#2895=VERTEX_POINT('',#9500);
#2896=VERTEX_POINT('',#9502);
#2897=VERTEX_POINT('',#9504);
#2898=VERTEX_POINT('',#9508);
#2899=VERTEX_POINT('',#9512);
#2900=VERTEX_POINT('',#9516);
#2901=VERTEX_POINT('',#9520);
#2902=VERTEX_POINT('',#9535);
#2903=VERTEX_POINT('',#9537);
#3509=EDGE_CURVE('',#2888,#2889,#252,.T.);
#3510=EDGE_CURVE('',#2890,#2888,#253,.T.);
#3511=EDGE_CURVE('',#2890,#2891,#1775,.T.);
#3512=EDGE_CURVE('',#2891,#2891,#2523,.T.);
#3513=EDGE_CURVE('',#2892,#2890,#254,.T.);
#3514=EDGE_CURVE('',#2893,#2892,#255,.T.);
#3515=EDGE_CURVE('',#2894,#2893,#256,.T.);
#3516=EDGE_CURVE('',#2889,#2894,#257,.T.);
#3517=EDGE_CURVE('',#2895,#2895,#2524,.T.);
#3518=EDGE_CURVE('',#2895,#2896,#1776,.T.);
#3519=EDGE_CURVE('',#2897,#2896,#258,.T.);
#3520=EDGE_CURVE('',#2898,#2897,#259,.T.);
#3521=EDGE_CURVE('',#2899,#2898,#260,.T.);
#3522=EDGE_CURVE('',#2900,#2899,#261,.T.);
#3523=EDGE_CURVE('',#2901,#2900,#262,.T.);
#3524=EDGE_CURVE('',#2896,#2901,#263,.T.);
#3525=EDGE_CURVE('',#2892,#2901,#1777,.T.);
#3526=EDGE_CURVE('',#2893,#2900,#1778,.T.);
#3527=EDGE_CURVE('',#2890,#2896,#1779,.T.);
#3528=EDGE_CURVE('',#2888,#2897,#1780,.T.);
#3529=EDGE_CURVE('',#2902,#2902,#2525,.F.);
#3530=EDGE_CURVE('',#2902,#2903,#1781,.T.);
#3531=EDGE_CURVE('',#2903,#2903,#2526,.F.);
#3532=EDGE_CURVE('',#2889,#2898,#1782,.T.);
#3533=EDGE_CURVE('',#2894,#2899,#1783,.T.);
#4685=ORIENTED_EDGE('',*,*,#3509,.F.);
#4686=ORIENTED_EDGE('',*,*,#3510,.F.);
#4687=ORIENTED_EDGE('',*,*,#3511,.T.);
#4688=ORIENTED_EDGE('',*,*,#3512,.F.);
#4689=ORIENTED_EDGE('',*,*,#3511,.F.);
#4690=ORIENTED_EDGE('',*,*,#3513,.F.);
#4691=ORIENTED_EDGE('',*,*,#3514,.F.);
#4692=ORIENTED_EDGE('',*,*,#3515,.F.);
#4693=ORIENTED_EDGE('',*,*,#3516,.F.);
#4694=ORIENTED_EDGE('',*,*,#3517,.F.);
#4695=ORIENTED_EDGE('',*,*,#3518,.T.);
#4696=ORIENTED_EDGE('',*,*,#3519,.F.);
#4697=ORIENTED_EDGE('',*,*,#3520,.F.);
#4698=ORIENTED_EDGE('',*,*,#3521,.F.);
#4699=ORIENTED_EDGE('',*,*,#3522,.F.);
#4700=ORIENTED_EDGE('',*,*,#3523,.F.);
#4701=ORIENTED_EDGE('',*,*,#3524,.F.);
#4702=ORIENTED_EDGE('',*,*,#3518,.F.);
#4703=ORIENTED_EDGE('',*,*,#3514,.T.);
#4704=ORIENTED_EDGE('',*,*,#3525,.T.);
#4705=ORIENTED_EDGE('',*,*,#3523,.T.);
#4706=ORIENTED_EDGE('',*,*,#3526,.F.);
#4707=ORIENTED_EDGE('',*,*,#3513,.T.);
#4708=ORIENTED_EDGE('',*,*,#3527,.T.);
#4709=ORIENTED_EDGE('',*,*,#3524,.T.);
#4710=ORIENTED_EDGE('',*,*,#3525,.F.);
#4711=ORIENTED_EDGE('',*,*,#3510,.T.);
#4712=ORIENTED_EDGE('',*,*,#3528,.T.);
#4713=ORIENTED_EDGE('',*,*,#3519,.T.);
#4714=ORIENTED_EDGE('',*,*,#3527,.F.);
#4715=ORIENTED_EDGE('',*,*,#3529,.F.);
#4716=ORIENTED_EDGE('',*,*,#3530,.T.);
#4717=ORIENTED_EDGE('',*,*,#3531,.T.);
#4718=ORIENTED_EDGE('',*,*,#3530,.F.);
#4719=ORIENTED_EDGE('',*,*,#3509,.T.);
#4720=ORIENTED_EDGE('',*,*,#3532,.T.);
#4721=ORIENTED_EDGE('',*,*,#3520,.T.);
#4722=ORIENTED_EDGE('',*,*,#3528,.F.);
#4723=ORIENTED_EDGE('',*,*,#3515,.T.);
#4724=ORIENTED_EDGE('',*,*,#3526,.T.);
#4725=ORIENTED_EDGE('',*,*,#3522,.T.);
#4726=ORIENTED_EDGE('',*,*,#3533,.F.);
#4727=ORIENTED_EDGE('',*,*,#3516,.T.);
#4728=ORIENTED_EDGE('',*,*,#3533,.T.);
#4729=ORIENTED_EDGE('',*,*,#3521,.T.);
#4730=ORIENTED_EDGE('',*,*,#3532,.F.);
#4731=ORIENTED_EDGE('',*,*,#3517,.T.);
#4732=ORIENTED_EDGE('',*,*,#3529,.T.);
#4733=ORIENTED_EDGE('',*,*,#3512,.T.);
#4734=ORIENTED_EDGE('',*,*,#3531,.F.);
#5231=CYLINDRICAL_SURFACE('',#6337,0.2117);
#5464=ADVANCED_FACE('',(#964),#270,.T.);
#5465=ADVANCED_FACE('',(#965),#271,.T.);
#5466=ADVANCED_FACE('',(#966),#660,.T.);
#5467=ADVANCED_FACE('',(#967),#661,.T.);
#5468=ADVANCED_FACE('',(#968),#662,.T.);
#5469=ADVANCED_FACE('',(#969),#5231,.F.);
#5470=ADVANCED_FACE('',(#970),#663,.T.);
#5471=ADVANCED_FACE('',(#971),#664,.T.);
#5472=ADVANCED_FACE('',(#972),#665,.T.);
#5473=ADVANCED_FACE('',(#973,#517),#666,.T.);
#5474=ADVANCED_FACE('',(#974,#518),#667,.F.);
#5595=CLOSED_SHELL('',(#5464,#5465,#5466,#5467,#5468,#5469,#5470,#5471,
#5472,#5473,#5474));
#6329=AXIS2_PLACEMENT_3D('',#9470,#7692,#7693);
#6330=AXIS2_PLACEMENT_3D('',#9471,#7694,#7695);
#6331=AXIS2_PLACEMENT_3D('',#9483,#7697,#7698);
#6332=AXIS2_PLACEMENT_3D('',#9499,#7699,#7700);
#6333=AXIS2_PLACEMENT_3D('',#9501,#7701,#7702);
#6334=AXIS2_PLACEMENT_3D('',#9527,#7704,#7705);
#6335=AXIS2_PLACEMENT_3D('',#9530,#7708,#7709);
#6336=AXIS2_PLACEMENT_3D('',#9532,#7711,#7712);
#6337=AXIS2_PLACEMENT_3D('',#9534,#7714,#7715);
#6338=AXIS2_PLACEMENT_3D('',#9536,#7716,#7717);
#6339=AXIS2_PLACEMENT_3D('',#9539,#7719,#7720);
#6340=AXIS2_PLACEMENT_3D('',#9540,#7721,#7722);
#6341=AXIS2_PLACEMENT_3D('',#9542,#7724,#7725);
#6342=AXIS2_PLACEMENT_3D('',#9544,#7727,#7728);
#6343=AXIS2_PLACEMENT_3D('',#9545,#7729,#7730);
#6344=AXIS2_PLACEMENT_3D('',#9546,#7731,#7732);
#7692=DIRECTION('axis',(0.,0.,1.));
#7693=DIRECTION('refdir',(1.,0.,0.));
#7694=DIRECTION('center_axis',(0.,1.,0.));
#7695=DIRECTION('ref_axis',(1.,0.,0.));
#7696=DIRECTION('',(0.866025403784439,-0.5,1.06057523872491E-16));
#7697=DIRECTION('center_axis',(0.,-1.,0.));
#7698=DIRECTION('ref_axis',(1.,0.,0.));
#7699=DIRECTION('center_axis',(0.,-1.,0.));
#7700=DIRECTION('ref_axis',(1.,0.,0.));
#7701=DIRECTION('center_axis',(0.,1.,0.));
#7702=DIRECTION('ref_axis',(1.,0.,0.));
#7703=DIRECTION('',(-0.866025403784439,-0.5,-1.06057523872491E-16));
#7704=DIRECTION('center_axis',(1.20185167898973E-16,0.,-1.));
#7705=DIRECTION('ref_axis',(-1.,0.,-1.20185167898973E-16));
#7706=DIRECTION('',(0.,1.,0.));
#7707=DIRECTION('',(0.,1.,0.));
#7708=DIRECTION('center_axis',(-0.866025403784439,0.,-0.5));
#7709=DIRECTION('ref_axis',(-0.5,0.,0.866025403784439));
#7710=DIRECTION('',(0.,1.,0.));
#7711=DIRECTION('center_axis',(-0.866025403784439,0.,0.5));
#7712=DIRECTION('ref_axis',(0.5,0.,0.866025403784439));
#7713=DIRECTION('',(0.,1.,0.));
#7714=DIRECTION('center_axis',(0.,1.,0.));
#7715=DIRECTION('ref_axis',(1.,0.,0.));
#7716=DIRECTION('center_axis',(0.,1.,0.));
#7717=DIRECTION('ref_axis',(1.,0.,0.));
#7718=DIRECTION('',(0.,-1.,0.));
#7719=DIRECTION('center_axis',(0.,1.,0.));
#7720=DIRECTION('ref_axis',(1.,0.,0.));
#7721=DIRECTION('center_axis',(-2.40370335797945E-16,0.,1.));
#7722=DIRECTION('ref_axis',(1.,0.,2.40370335797945E-16));
#7723=DIRECTION('',(0.,1.,0.));
#7724=DIRECTION('center_axis',(0.866025403784439,0.,-0.5));
#7725=DIRECTION('ref_axis',(-0.5,0.,-0.866025403784439));
#7726=DIRECTION('',(0.,1.,0.));
#7727=DIRECTION('center_axis',(0.866025403784439,0.,0.5));
#7728=DIRECTION('ref_axis',(0.5,0.,-0.866025403784439));
#7729=DIRECTION('center_axis',(0.,1.,0.));
#7730=DIRECTION('ref_axis',(1.,0.,0.));
#7731=DIRECTION('center_axis',(0.,1.,0.));
#7732=DIRECTION('ref_axis',(1.,0.,0.));
#9470=CARTESIAN_POINT('',(0.,0.,0.));
#9471=CARTESIAN_POINT('Origin',(0.,0.0525042956467857,0.));
#9472=CARTESIAN_POINT('',(-0.230940107675851,0.0472735643746089,0.4));
#9473=CARTESIAN_POINT('',(0.23094010767585,0.0472735643746089,0.4));
#9474=CARTESIAN_POINT('Ctrl Pts',(-0.230940107675851,0.0472735643746089,
0.4));
#9475=CARTESIAN_POINT('Ctrl Pts',(1.11022302462516E-16,-0.0193931022920578,
0.4));
#9476=CARTESIAN_POINT('Ctrl Pts',(0.23094010767585,0.0472735643746089,0.4));
#9477=CARTESIAN_POINT('',(-0.461880215351701,0.0472735643746089,-5.6564012731995E-17));
#9478=CARTESIAN_POINT('Ctrl Pts',(-0.461880215351701,0.0472735643746089,
-5.6564012731995E-17));
#9479=CARTESIAN_POINT('Ctrl Pts',(-0.346410161513776,-0.0193931022920579,
0.2));
#9480=CARTESIAN_POINT('Ctrl Pts',(-0.230940107675851,0.0472735643746089,
0.4));
#9481=CARTESIAN_POINT('',(-0.38,-2.08166817117217E-17,-4.65365783675994E-17));
#9482=CARTESIAN_POINT('',(-0.47094010767585,0.0525042956467857,-5.7673529545534E-17));
#9483=CARTESIAN_POINT('Origin',(0.,0.,0.));
#9484=CARTESIAN_POINT('',(-0.23094010767585,0.0472735643746089,-0.4));
#9485=CARTESIAN_POINT('Ctrl Pts',(-0.23094010767585,0.0472735643746089,
-0.4));
#9486=CARTESIAN_POINT('Ctrl Pts',(-0.346410161513775,-0.0193931022920578,
-0.2));
#9487=CARTESIAN_POINT('Ctrl Pts',(-0.461880215351701,0.0472735643746089,
-5.6564012731995E-17));
#9488=CARTESIAN_POINT('',(0.23094010767585,0.0472735643746089,-0.4));
#9489=CARTESIAN_POINT('Ctrl Pts',(0.23094010767585,0.0472735643746089,-0.4));
#9490=CARTESIAN_POINT('Ctrl Pts',(0.,-0.0193931022920578,-0.4));
#9491=CARTESIAN_POINT('Ctrl Pts',(-0.23094010767585,0.0472735643746089,
-0.4));
#9492=CARTESIAN_POINT('',(0.461880215351701,0.0472735643746089,0.));
#9493=CARTESIAN_POINT('Ctrl Pts',(0.461880215351701,0.0472735643746089,
0.));
#9494=CARTESIAN_POINT('Ctrl Pts',(0.346410161513776,-0.019393102292058,
-0.2));
#9495=CARTESIAN_POINT('Ctrl Pts',(0.23094010767585,0.0472735643746089,-0.4));
#9496=CARTESIAN_POINT('Ctrl Pts',(0.23094010767585,0.0472735643746089,0.4));
#9497=CARTESIAN_POINT('Ctrl Pts',(0.346410161513776,-0.0193931022920577,
0.2));
#9498=CARTESIAN_POINT('Ctrl Pts',(0.461880215351701,0.0472735643746089,
0.));
#9499=CARTESIAN_POINT('Origin',(0.,0.417495704353214,0.));
#9500=CARTESIAN_POINT('',(-0.38,0.47,-4.65365783675994E-17));
#9501=CARTESIAN_POINT('Origin',(0.,0.47,0.));
#9502=CARTESIAN_POINT('',(-0.461880215351701,0.422726435625391,-5.6564012731995E-17));
#9503=CARTESIAN_POINT('',(-0.47094010767585,0.417495704353214,-5.7673529545534E-17));
#9504=CARTESIAN_POINT('',(-0.230940107675851,0.422726435625391,0.4));
#9505=CARTESIAN_POINT('Ctrl Pts',(-0.230940107675851,0.422726435625391,
0.4));
#9506=CARTESIAN_POINT('Ctrl Pts',(-0.346410161513776,0.489393102292058,
0.2));
#9507=CARTESIAN_POINT('Ctrl Pts',(-0.461880215351701,0.422726435625391,
-5.6564012731995E-17));
#9508=CARTESIAN_POINT('',(0.23094010767585,0.422726435625391,0.4));
#9509=CARTESIAN_POINT('Ctrl Pts',(0.23094010767585,0.422726435625391,0.4));
#9510=CARTESIAN_POINT('Ctrl Pts',(8.32667268468867E-17,0.489393102292058,
0.4));
#9511=CARTESIAN_POINT('Ctrl Pts',(-0.230940107675851,0.422726435625391,
0.4));
#9512=CARTESIAN_POINT('',(0.461880215351701,0.422726435625391,0.));
#9513=CARTESIAN_POINT('Ctrl Pts',(0.461880215351701,0.422726435625391,0.));
#9514=CARTESIAN_POINT('Ctrl Pts',(0.346410161513776,0.489393102292058,0.2));
#9515=CARTESIAN_POINT('Ctrl Pts',(0.23094010767585,0.422726435625391,0.4));
#9516=CARTESIAN_POINT('',(0.23094010767585,0.422726435625391,-0.4));
#9517=CARTESIAN_POINT('Ctrl Pts',(0.23094010767585,0.422726435625391,-0.4));
#9518=CARTESIAN_POINT('Ctrl Pts',(0.346410161513775,0.489393102292058,-0.2));
#9519=CARTESIAN_POINT('Ctrl Pts',(0.461880215351701,0.422726435625391,0.));
#9520=CARTESIAN_POINT('',(-0.23094010767585,0.422726435625391,-0.4));
#9521=CARTESIAN_POINT('Ctrl Pts',(-0.23094010767585,0.422726435625391,-0.4));
#9522=CARTESIAN_POINT('Ctrl Pts',(-5.55111512312578E-17,0.489393102292058,
-0.4));
#9523=CARTESIAN_POINT('Ctrl Pts',(0.23094010767585,0.422726435625391,-0.4));
#9524=CARTESIAN_POINT('Ctrl Pts',(-0.461880215351701,0.422726435625391,
-5.6564012731995E-17));
#9525=CARTESIAN_POINT('Ctrl Pts',(-0.346410161513776,0.489393102292058,
-0.2));
#9526=CARTESIAN_POINT('Ctrl Pts',(-0.23094010767585,0.422726435625391,-0.4));
#9527=CARTESIAN_POINT('Origin',(0.23094010767585,0.,-0.4));
#9528=CARTESIAN_POINT('',(-0.23094010767585,0.,-0.4));
#9529=CARTESIAN_POINT('',(0.23094010767585,0.,-0.4));
#9530=CARTESIAN_POINT('Origin',(-0.23094010767585,0.,-0.4));
#9531=CARTESIAN_POINT('',(-0.461880215351701,0.,-5.6564012731995E-17));
#9532=CARTESIAN_POINT('Origin',(-0.461880215351701,0.,-5.6564012731995E-17));
#9533=CARTESIAN_POINT('',(-0.230940107675851,0.,0.4));
#9534=CARTESIAN_POINT('Origin',(0.,0.,0.));
#9535=CARTESIAN_POINT('',(-0.2117,0.47,2.59257727379495E-17));
#9536=CARTESIAN_POINT('Origin',(0.,0.47,0.));
#9537=CARTESIAN_POINT('',(-0.2117,0.,2.59257727379495E-17));
#9538=CARTESIAN_POINT('',(-0.2117,0.,2.59257727379495E-17));
#9539=CARTESIAN_POINT('Origin',(0.,0.,0.));
#9540=CARTESIAN_POINT('Origin',(-0.230940107675851,0.,0.4));
#9541=CARTESIAN_POINT('',(0.23094010767585,0.,0.4));
#9542=CARTESIAN_POINT('Origin',(0.461880215351701,0.,0.));
#9543=CARTESIAN_POINT('',(0.461880215351701,0.,0.));
#9544=CARTESIAN_POINT('Origin',(0.23094010767585,0.,0.4));
#9545=CARTESIAN_POINT('Origin',(0.,0.47,0.));
#9546=CARTESIAN_POINT('Origin',(0.,0.,0.));
#10076=UNCERTAINTY_MEASURE_WITH_UNIT(LENGTH_MEASURE(0.001),#10120,
'DISTANCE_ACCURACY_VALUE',
'Maximum model space distance between geometric entities at asserted c
onnectivities');
#10088=UNCERTAINTY_MEASURE_WITH_UNIT(LENGTH_MEASURE(0.001),#10120,
'DISTANCE_ACCURACY_VALUE',
'Maximum model space distance between geometric entities at asserted c
onnectivities');
#10107=(
GEOMETRIC_REPRESENTATION_CONTEXT(3)
GLOBAL_UNCERTAINTY_ASSIGNED_CONTEXT((#10076))
GLOBAL_UNIT_ASSIGNED_CONTEXT((#10120,#10122,#10123))
REPRESENTATION_CONTEXT('','3D')
);
#10119=(
GEOMETRIC_REPRESENTATION_CONTEXT(3)
GLOBAL_UNCERTAINTY_ASSIGNED_CONTEXT((#10088))
GLOBAL_UNIT_ASSIGNED_CONTEXT((#10120,#10122,#10123))
REPRESENTATION_CONTEXT('','3D')
);
#10120=(
LENGTH_UNIT()
NAMED_UNIT(*)
SI_UNIT(.CENTI.,.METRE.)
);
#10122=(
NAMED_UNIT(*)
PLANE_ANGLE_UNIT()
SI_UNIT($,.RADIAN.)
);
#10123=(
NAMED_UNIT(*)
SI_UNIT($,.STERADIAN.)
SOLID_ANGLE_UNIT()
);
#10142=SHAPE_DEFINITION_REPRESENTATION(#10172,#10258);
#10172=PRODUCT_DEFINITION_SHAPE('',$,#10289);
#10258=SHAPE_REPRESENTATION('',(#6329),#10107);
#10270=PRODUCT_DEFINITION_CONTEXT('part definition',#10362,'design');
#10289=PRODUCT_DEFINITION('Hex Nut - M5','Hex Nut - M5',#10319,#10270);
#10319=PRODUCT_DEFINITION_FORMATION('',$,#10382);
#10362=APPLICATION_CONTEXT(
'Core Data for Automotive Mechanical Design Process');
#10363=PRODUCT_CONTEXT('part definition',#10362,'mechanical');
#10382=PRODUCT('Hex Nut - M5','Hex Nut - M5','Hex Nut - M5',(#10363));
#10471=COLOUR_RGB('Black',0.12,0.14,0.17);
#10472=FILL_AREA_STYLE_COLOUR('',#10471);
#10473=FILL_AREA_STYLE('',(#10472));
#10474=SURFACE_STYLE_FILL_AREA(#10473);
#10475=SURFACE_SIDE_STYLE('',(#10474));
#10476=SURFACE_STYLE_USAGE(.BOTH.,#10475);
#10477=PRESENTATION_STYLE_ASSIGNMENT((#10476));
ENDSEC;
END-ISO-10303-21;
